ISO-10303-21;
HEADER;
FILE_DESCRIPTION (('STEP AP214'),
    '1' );
FILE_NAME ('roller axis assy_r1.step',
    '2026-10-24T11:01:53',
    ( '' ),
    ( '' ),
    'SwSTEP 2.0',
    'SolidWorks 2026',
    '' );
FILE_SCHEMA (( 'AUTOMOTIVE_DESIGN' ));
ENDSEC;

DATA;
#8=ORIENTED_EDGE ( 'NONE', *, *, #6474, .F. ) ;
#21=LINE ( 'NONE', #519, #5740 ) ;
#32=ORIENTED_EDGE ( 'NONE', *, *, #8020, .T. ) ;
#42=DIRECTION ( 'NONE',  ( -0.000000000000000000, -0.000000000000000000, 1.000000000000000000 ) ) ;
#44=DIRECTION ( 'NONE',  ( -1.000000000000000000, 0.000000000000000000, 0.000000000000000000 ) ) ;
#47=CARTESIAN_POINT ( 'NONE',  ( 5.000000000000000000, -5.000000000000000000, 148.0000000000000284 ) ) ;
#81=VECTOR ( 'NONE', #7075, 1000.000000000000000 ) ;
#84=ORIENTED_EDGE ( 'NONE', *, *, #5741, .T. ) ;
#177=( GEOMETRIC_REPRESENTATION_CONTEXT ( 3 ) GLOBAL_UNCERTAINTY_ASSIGNED_CONTEXT ( ( #6671 ) ) GLOBAL_UNIT_ASSIGNED_CONTEXT ( ( #6629, #7289, #586 ) ) REPRESENTATION_CONTEXT ( 'NONE', 'WORKASPACE' ) );
#211=AXIS2_PLACEMENT_3D ( 'NONE', #7037, #7745, #1783 ) ;
#223=ADVANCED_FACE ( 'NONE', ( #1998, #2816 ), #373, .T. ) ;
#242=VERTEX_POINT ( 'NONE', #1553 ) ;
#251=DIRECTION ( 'NONE',  ( -0.000000000000000000, -0.000000000000000000, 1.000000000000000000 ) ) ;
#261=FACE_OUTER_BOUND ( 'NONE', #2202, .T. ) ;
#279=EDGE_CURVE ( 'NONE', #5674, #3807, #5550, .T. ) ;
#303=FACE_BOUND ( 'NONE', #4384, .T. ) ;
#308=AXIS2_PLACEMENT_3D ( 'NONE', #6873, #251, #6040 ) ;
#320=FACE_OUTER_BOUND ( 'NONE', #6882, .T. ) ;
#321=LINE ( 'NONE', #6328, #6444 ) ;
#326=CARTESIAN_POINT ( 'NONE',  ( 5.000000000000000000, -5.000000000000000000, -143.0000000000000284 ) ) ;
#329=ADVANCED_FACE ( 'NONE', ( #2350 ), #2992, .T. ) ;
#340=PLANE ( 'NONE',  #5145 ) ;
#346=CARTESIAN_POINT ( 'NONE',  ( 5.000000000000000000, 5.000000000000000000, 140.0000000000000000 ) ) ;
#348=PLANE ( 'NONE',  #2219 ) ;
#352=CARTESIAN_POINT ( 'NONE',  ( -5.000000000000001776, 5.000000000000001776, -135.0000000000000000 ) ) ;
#373=PLANE ( 'NONE',  #8303 ) ;
#385=ORIENTED_EDGE ( 'NONE', *, *, #7155, .F. ) ;
#395=ORIENTED_EDGE ( 'NONE', *, *, #4970, .F. ) ;
#438=DIRECTION ( 'NONE',  ( -1.000000000000000000, 0.000000000000000000, -0.000000000000000000 ) ) ;
#440=PRODUCT_DEFINITION_FORMATION_WITH_SPECIFIED_SOURCE ( 'ANY', '', #7953, .NOT_KNOWN. ) ;
#450=EDGE_CURVE ( 'NONE', #2803, #5343, #1779, .T. ) ;
#464=DIRECTION ( 'NONE',  ( 0.000000000000000000, 0.000000000000000000, 1.000000000000000000 ) ) ;
#470=LINE ( 'NONE', #7746, #7853 ) ;
#481=CARTESIAN_POINT ( 'NONE',  ( -10.00000000000000000, 1.224646799147353256E-15, -115.0000000000000000 ) ) ;
#484=ADVANCED_FACE ( 'NONE', ( #5765 ), #2597, .F. ) ;
#491=EDGE_CURVE ( 'NONE', #1367, #1428, #5842, .T. ) ;
#504=ORIENTED_EDGE ( 'NONE', *, *, #6187, .T. ) ;
#515=CARTESIAN_POINT ( 'NONE',  ( 0.000000000000000000, 0.000000000000000000, -191.5685424949238325 ) ) ;
#519=CARTESIAN_POINT ( 'NONE',  ( 5.000000000000000000, 5.000000000000000000, -143.0000000000000284 ) ) ;
#537=CYLINDRICAL_SURFACE ( 'NONE', #7711, 10.00000000000000000 ) ;
#559=CARTESIAN_POINT ( 'NONE',  ( -5.000000000000001776, 5.000000000000001776, 140.0000000000000000 ) ) ;
#571=DIRECTION ( 'NONE',  ( -0.000000000000000000, -0.000000000000000000, 1.000000000000000000 ) ) ;
#586=( NAMED_UNIT ( * ) SI_UNIT ( $, .STERADIAN. ) SOLID_ANGLE_UNIT ( ) );
#594=AXIS2_PLACEMENT_3D ( 'NONE', #3123, #464, #5764 ) ;
#605=CARTESIAN_POINT ( 'NONE',  ( 5.000000000000000000, -5.000000000000000000, -143.0000000000000284 ) ) ;
#617=DIRECTION ( 'NONE',  ( 0.000000000000000000, -1.000000000000000000, 0.000000000000000000 ) ) ;
#647=VECTOR ( 'NONE', #2635, 1000.000000000000000 ) ;
#660=DIRECTION ( 'NONE',  ( 1.000000000000000000, 0.000000000000000000, 0.000000000000000000 ) ) ;
#663=ORIENTED_EDGE ( 'NONE', *, *, #3639, .T. ) ;
#666=EDGE_CURVE ( 'NONE', #242, #2803, #2187, .T. ) ;
#669=DIRECTION ( 'NONE',  ( 1.734723475976806848E-16, -1.000000000000000000, -0.000000000000000000 ) ) ;
#700=CARTESIAN_POINT ( 'NONE',  ( 5.000000000000000000, 5.000000000000000000, -143.0000000000000284 ) ) ;
#704=EDGE_CURVE ( 'NONE', #3882, #5674, #2793, .T. ) ;
#708=ADVANCED_FACE ( 'NONE', ( #7273 ), #6614, .F. ) ;
#747=DIRECTION ( 'NONE',  ( -0.000000000000000000, -0.000000000000000000, -1.000000000000000000 ) ) ;
#754=ORIENTED_EDGE ( 'NONE', *, *, #3538, .T. ) ;
#762=CARTESIAN_POINT ( 'NONE',  ( 5.000000000000000000, 5.000000000000000000, -143.0000000000000284 ) ) ;
#767=UNCERTAINTY_MEASURE_WITH_UNIT (LENGTH_MEASURE( 1.000000000000000082E-05 ), #3325, 'distance_accuracy_value', 'NONE');
#773=ORIENTED_EDGE ( 'NONE', *, *, #4245, .T. ) ;
#816=SHAPE_DEFINITION_REPRESENTATION ( #8175, #1533 ) ;
#824=ADVANCED_FACE ( 'NONE', ( #303, #3493 ), #7627, .T. ) ;
#840=VECTOR ( 'NONE', #844, 1000.000000000000000 ) ;
#844=DIRECTION ( 'NONE',  ( -1.000000000000000000, 1.734723475976806848E-16, -0.000000000000000000 ) ) ;
#847=ORIENTED_EDGE ( 'NONE', *, *, #450, .T. ) ;
#909=ORIENTED_EDGE ( 'NONE', *, *, #279, .T. ) ;
#949=DIRECTION ( 'NONE',  ( 0.000000000000000000, 0.000000000000000000, 1.000000000000000000 ) ) ;
#966=AXIS2_PLACEMENT_3D ( 'NONE', #6013, #2106, #2634 ) ;
#971=AXIS2_PLACEMENT_3D ( 'NONE', #2426, #571, #8551 ) ;
#1033=VERTEX_POINT ( 'NONE', #4401 ) ;
#1043=EDGE_CURVE ( 'NONE', #3807, #1428, #7052, .T. ) ;
#1056=ORIENTED_EDGE ( 'NONE', *, *, #1919, .T. ) ;
#1080=CARTESIAN_POINT ( 'NONE',  ( 5.000000000000000000, -5.000000000000000000, 140.0000000000000000 ) ) ;
#1095=CARTESIAN_POINT ( 'NONE',  ( -5.000000000000000000, -5.000000000000000000, -143.0000000000000284 ) ) ;
#1102=CIRCLE ( 'NONE', #966, 10.00000000000000000 ) ;
#1111=DIRECTION ( 'NONE',  ( -1.000000000000000000, 0.000000000000000000, -0.000000000000000000 ) ) ;
#1131=ORIENTED_EDGE ( 'NONE', *, *, #6482, .F. ) ;
#1133=CARTESIAN_POINT ( 'NONE',  ( 5.000000000000000000, 5.000000000000000000, -135.0000000000000000 ) ) ;
#1151=VECTOR ( 'NONE', #7357, 1000.000000000000000 ) ;
#1163=ORIENTED_EDGE ( 'NONE', *, *, #4970, .T. ) ;
#1167=( GEOMETRIC_REPRESENTATION_CONTEXT ( 3 ) GLOBAL_UNCERTAINTY_ASSIGNED_CONTEXT ( ( #7375 ) ) GLOBAL_UNIT_ASSIGNED_CONTEXT ( ( #5199, #5155, #8515 ) ) REPRESENTATION_CONTEXT ( 'NONE', 'WORKASPACE' ) );
#1196=CARTESIAN_POINT ( 'NONE',  ( -10.00000000000000000, 1.224646799147353256E-15, -135.0000000000000000 ) ) ;
#1216=EDGE_LOOP ( 'NONE', ( #2370, #6915, #754, #504 ) ) ;
#1224=ORIENTED_EDGE ( 'NONE', *, *, #7346, .T. ) ;
#1225=CARTESIAN_POINT ( 'NONE',  ( 5.000000000000000000, 5.000000000000000000, -135.0000000000000000 ) ) ;
#1229=CARTESIAN_POINT ( 'NONE',  ( 0.000000000000000000, 0.000000000000000000, 140.0000000000000000 ) ) ;
#1231=CARTESIAN_POINT ( 'NONE',  ( -5.000000000000001776, 5.000000000000001776, -135.0000000000000000 ) ) ;
#1238=SURFACE_STYLE_USAGE ( .BOTH. , #3817 ) ;
#1290=EDGE_LOOP ( 'NONE', ( #5691, #2012 ) ) ;
#1302=AXIS2_PLACEMENT_3D ( 'NONE', #5543, #5456, #8086 ) ;
#1304=CARTESIAN_POINT ( 'NONE',  ( 10.00000000000000000, 0.000000000000000000, 120.0000000000000000 ) ) ;
#1327=CARTESIAN_POINT ( 'NONE',  ( 5.000000000000000000, -5.000000000000000000, 140.0000000000000000 ) ) ;
#1367=VERTEX_POINT ( 'NONE', #3779 ) ;
#1393=ORIENTED_EDGE ( 'NONE', *, *, #4033, .T. ) ;
#1402=DIRECTION ( 'NONE',  ( 0.000000000000000000, 0.000000000000000000, -1.000000000000000000 ) ) ;
#1403=LINE ( 'NONE', #8079, #4480 ) ;
#1425=PRODUCT_CONTEXT ( 'NONE', #2585, 'mechanical' ) ;
#1428=VERTEX_POINT ( 'NONE', #5728 ) ;
#1444=CARTESIAN_POINT ( 'NONE',  ( 0.000000000000000000, 0.000000000000000000, 148.0000000000000284 ) ) ;
#1467=ORIENTED_EDGE ( 'NONE', *, *, #7367, .F. ) ;
#1473=ADVANCED_FACE ( 'NONE', ( #2644 ), #6548, .F. ) ;
#1498=FACE_OUTER_BOUND ( 'NONE', #3641, .T. ) ;
#1510=CARTESIAN_POINT ( 'NONE',  ( 0.000000000000000000, 0.000000000000000000, -135.0000000000000000 ) ) ;
#1533=SHAPE_REPRESENTATION ( 'roller axis assy_r1', ( #594 ), #1167 ) ;
#1552=CYLINDRICAL_SURFACE ( 'NONE', #4351, 10.00000000000000000 ) ;
#1553=CARTESIAN_POINT ( 'NONE',  ( -10.00000000000000000, 1.224646799147353256E-15, 120.0000000000000000 ) ) ;
#1566=AXIS2_PLACEMENT_3D ( 'NONE', #2885, #4144, #4276 ) ;
#1585=CARTESIAN_POINT ( 'NONE',  ( -5.000000000000001776, 5.000000000000001776, 148.0000000000000284 ) ) ;
#1599=VERTEX_POINT ( 'NONE', #3598 ) ;
#1600=DIRECTION ( 'NONE',  ( 1.000000000000000000, 0.000000000000000000, 0.000000000000000000 ) ) ;
#1606=CARTESIAN_POINT ( 'NONE',  ( 0.000000000000000000, 0.000000000000000000, -135.0000000000000000 ) ) ;
#1661=ORIENTED_EDGE ( 'NONE', *, *, #1043, .F. ) ;
#1664=AXIS2_PLACEMENT_3D ( 'NONE', #6665, #3369, #6585 ) ;
#1666=DIRECTION ( 'NONE',  ( 1.000000000000000000, 0.000000000000000000, -0.000000000000000000 ) ) ;
#1668=ORIENTED_EDGE ( 'NONE', *, *, #6242, .F. ) ;
#1673=DIRECTION ( 'NONE',  ( 1.000000000000000000, 1.734723475976806848E-16, 0.000000000000000000 ) ) ;
#1674=AXIS2_PLACEMENT_3D ( 'NONE', #47, #3943, #3457 ) ;
#1687=ORIENTED_EDGE ( 'NONE', *, *, #3454, .T. ) ;
#1715=ORIENTED_EDGE ( 'NONE', *, *, #4826, .T. ) ;
#1722=DIRECTION ( 'NONE',  ( -1.000000000000000000, 0.000000000000000000, 0.000000000000000000 ) ) ;
#1734=DIRECTION ( 'NONE',  ( -1.000000000000000000, 0.000000000000000000, 0.000000000000000000 ) ) ;
#1768=AXIS2_PLACEMENT_3D ( 'NONE', #5592, #949, #1600 ) ;
#1777=ORIENTED_EDGE ( 'NONE', *, *, #3453, .F. ) ;
#1779=LINE ( 'NONE', #5156, #81 ) ;
#1781=VERTEX_POINT ( 'NONE', #6419 ) ;
#1783=DIRECTION ( 'NONE',  ( 1.000000000000000000, 0.000000000000000000, 0.000000000000000000 ) ) ;
#1817=ORIENTED_EDGE ( 'NONE', *, *, #3453, .T. ) ;
#1826=LINE ( 'NONE', #4468, #2555 ) ;
#1893=LINE ( 'NONE', #7103, #7080 ) ;
#1898=CARTESIAN_POINT ( 'NONE',  ( -5.000000000000001776, 5.000000000000001776, -143.0000000000000284 ) ) ;
#1919=EDGE_CURVE ( 'NONE', #7049, #3079, #3246, .T. ) ;
#1948=AXIS2_PLACEMENT_3D ( 'NONE', #1229, #8426, #1722 ) ;
#1998=FACE_BOUND ( 'NONE', #4292, .T. ) ;
#2008=CIRCLE ( 'NONE', #6858, 10.00000000000000000 ) ;
#2012=ORIENTED_EDGE ( 'NONE', *, *, #5741, .F. ) ;
#2050=AXIS2_PLACEMENT_3D ( 'NONE', #1444, #5307, #4794 ) ;
#2072=ORIENTED_EDGE ( 'NONE', *, *, #2603, .T. ) ;
#2106=DIRECTION ( 'NONE',  ( 0.000000000000000000, 0.000000000000000000, -1.000000000000000000 ) ) ;
#2107=ORIENTED_EDGE ( 'NONE', *, *, #7155, .T. ) ;
#2123=ORIENTED_EDGE ( 'NONE', *, *, #7795, .F. ) ;
#2137=COLOUR_RGB ( '',0.8941176470588234615, 0.8941176470588234615, 0.8941176470588234615 ) ;
#2144=AXIS2_PLACEMENT_3D ( 'NONE', #2768, #3419, #6854 ) ;
#2147=EDGE_LOOP ( 'NONE', ( #4820, #3136, #8, #6022 ) ) ;
#2183=EDGE_LOOP ( 'NONE', ( #2863, #2072 ) ) ;
#2187=CIRCLE ( 'NONE', #6212, 10.00000000000000000 ) ;
#2202=EDGE_LOOP ( 'NONE', ( #32, #7144, #1467, #5379 ) ) ;
#2219=AXIS2_PLACEMENT_3D ( 'NONE', #6315, #2882, #4843 ) ;
#2329=ORIENTED_EDGE ( 'NONE', *, *, #6482, .T. ) ;
#2350=FACE_OUTER_BOUND ( 'NONE', #6123, .T. ) ;
#2370=ORIENTED_EDGE ( 'NONE', *, *, #5126, .F. ) ;
#2391=ORIENTED_EDGE ( 'NONE', *, *, #7367, .T. ) ;
#2395=ORIENTED_EDGE ( 'NONE', *, *, #666, .T. ) ;
#2405=ORIENTED_EDGE ( 'NONE', *, *, #6103, .T. ) ;
#2420=CARTESIAN_POINT ( 'NONE',  ( 0.000000000000000000, 0.000000000000000000, -143.0000000000000284 ) ) ;
#2426=CARTESIAN_POINT ( 'NONE',  ( 0.000000000000000000, 0.000000000000000000, -115.0000000000000000 ) ) ;
#2461=ORIENTED_EDGE ( 'NONE', *, *, #4826, .F. ) ;
#2465=CARTESIAN_POINT ( 'NONE',  ( 5.000000000000000000, -5.000000000000000000, 148.0000000000000284 ) ) ;
#2466=DIRECTION ( 'NONE',  ( -0.000000000000000000, -0.000000000000000000, 1.000000000000000000 ) ) ;
#2473=LINE ( 'NONE', #1231, #6450 ) ;
#2479=DIRECTION ( 'NONE',  ( -1.000000000000000000, 0.000000000000000000, 0.000000000000000000 ) ) ;
#2517=DIRECTION ( 'NONE',  ( 0.000000000000000000, 1.000000000000000000, 0.000000000000000000 ) ) ;
#2549=AXIS2_PLACEMENT_3D ( 'NONE', #4576, #1402, #44 ) ;
#2552=DIRECTION ( 'NONE',  ( 1.000000000000000000, 0.000000000000000000, 0.000000000000000000 ) ) ;
#2555=VECTOR ( 'NONE', #3733, 1000.000000000000000 ) ;
#2562=DIRECTION ( 'NONE',  ( 0.000000000000000000, -0.000000000000000000, 1.000000000000000000 ) ) ;
#2578=CARTESIAN_POINT ( 'NONE',  ( -5.000000000000000000, -5.000000000000000000, 148.0000000000000284 ) ) ;
#2579=ORIENTED_EDGE ( 'NONE', *, *, #4168, .T. ) ;
#2585=APPLICATION_CONTEXT ( 'automotive_design' ) ;
#2586=( NAMED_UNIT ( * ) PLANE_ANGLE_UNIT ( ) SI_UNIT ( $, .RADIAN. ) );
#2596=EDGE_LOOP ( 'NONE', ( #1224, #385, #3516, #2405 ) ) ;
#2597=PLANE ( 'NONE',  #4680 ) ;
#2603=EDGE_CURVE ( 'NONE', #3079, #2989, #2898, .T. ) ;
#2613=CARTESIAN_POINT ( 'NONE',  ( 0.000000000000000000, 0.000000000000000000, -115.0000000000000000 ) ) ;
#2634=DIRECTION ( 'NONE',  ( -1.000000000000000000, 0.000000000000000000, 0.000000000000000000 ) ) ;
#2635=DIRECTION ( 'NONE',  ( 0.000000000000000000, 0.000000000000000000, 1.000000000000000000 ) ) ;
#2644=FACE_OUTER_BOUND ( 'NONE', #4907, .T. ) ;
#2732=VERTEX_POINT ( 'NONE', #346 ) ;
#2740=DIRECTION ( 'NONE',  ( -1.000000000000000000, 0.000000000000000000, -0.000000000000000000 ) ) ;
#2753=CARTESIAN_POINT ( 'NONE',  ( 0.000000000000000000, 0.000000000000000000, 120.0000000000000000 ) ) ;
#2766=ORIENTED_EDGE ( 'NONE', *, *, #704, .F. ) ;
#2768=CARTESIAN_POINT ( 'NONE',  ( 0.000000000000000000, 0.000000000000000000, -115.0000000000000000 ) ) ;
#2793=LINE ( 'NONE', #700, #7324 ) ;
#2803=VERTEX_POINT ( 'NONE', #1304 ) ;
#2805=VERTEX_POINT ( 'NONE', #2578 ) ;
#2816=FACE_OUTER_BOUND ( 'NONE', #7024, .T. ) ;
#2820=AXIS2_PLACEMENT_3D ( 'NONE', #2420, #5055, #438 ) ;
#2821=ORIENTED_EDGE ( 'NONE', *, *, #491, .T. ) ;
#2822=CARTESIAN_POINT ( 'NONE',  ( 0.000000000000000000, 0.000000000000000000, 140.0000000000000000 ) ) ;
#2823=LINE ( 'NONE', #8230, #3944 ) ;
#2856=ORIENTED_EDGE ( 'NONE', *, *, #6529, .F. ) ;
#2860=APPLICATION_CONTEXT ( 'automotive_design' ) ;
#2863=ORIENTED_EDGE ( 'NONE', *, *, #6242, .T. ) ;
#2882=DIRECTION ( 'NONE',  ( 0.000000000000000000, 1.000000000000000000, 0.000000000000000000 ) ) ;
#2885=CARTESIAN_POINT ( 'NONE',  ( 0.000000000000000000, 0.000000000000000000, 120.0000000000000000 ) ) ;
#2898=CIRCLE ( 'NONE', #7065, 20.00000000000000000 ) ;
#2908=DIRECTION ( 'NONE',  ( -0.000000000000000000, -0.000000000000000000, -1.000000000000000000 ) ) ;
#2915=ORIENTED_EDGE ( 'NONE', *, *, #7146, .F. ) ;
#2989=VERTEX_POINT ( 'NONE', #8062 ) ;
#2992=CYLINDRICAL_SURFACE ( 'NONE', #1768, 20.00000000000000000 ) ;
#2994=ORIENTED_EDGE ( 'NONE', *, *, #8204, .T. ) ;
#3002=CARTESIAN_POINT ( 'NONE',  ( 0.000000000000000000, 0.000000000000000000, 140.0000000000000000 ) ) ;
#3018=FACE_OUTER_BOUND ( 'NONE', #3863, .T. ) ;
#3040=CARTESIAN_POINT ( 'NONE',  ( 0.000000000000000000, 0.000000000000000000, -135.0000000000000000 ) ) ;
#3079=VERTEX_POINT ( 'NONE', #5604 ) ;
#3096=CIRCLE ( 'NONE', #2549, 10.00000000000000000 ) ;
#3123=CARTESIAN_POINT ( 'NONE',  ( 0.000000000000000000, 0.000000000000000000, 0.000000000000000000 ) ) ;
#3128=AXIS2_PLACEMENT_3D ( 'NONE', #2613, #5254, #2740 ) ;
#3136=ORIENTED_EDGE ( 'NONE', *, *, #8020, .F. ) ;
#3169=DIRECTION ( 'NONE',  ( -0.000000000000000000, -0.000000000000000000, -1.000000000000000000 ) ) ;
#3174=DIRECTION ( 'NONE',  ( 0.000000000000000000, 0.000000000000000000, 1.000000000000000000 ) ) ;
#3191=ADVANCED_FACE ( 'NONE', ( #3458 ), #6710, .T. ) ;
#3194=EDGE_CURVE ( 'NONE', #1033, #4010, #1102, .T. ) ;
#3200=DIRECTION ( 'NONE',  ( -0.000000000000000000, -0.000000000000000000, 1.000000000000000000 ) ) ;
#3206=ORIENTED_EDGE ( 'NONE', *, *, #7605, .F. ) ;
#3212=DIRECTION ( 'NONE',  ( -1.734723475976806848E-16, 1.000000000000000000, 0.000000000000000000 ) ) ;
#3246=LINE ( 'NONE', #7959, #647 ) ;
#3273=ADVANCED_FACE ( 'NONE', ( #1498 ), #3413, .F. ) ;
#3278=DIRECTION ( 'NONE',  ( -1.734723475976806848E-16, -1.000000000000000000, 0.000000000000000000 ) ) ;
#3280=DIRECTION ( 'NONE',  ( 1.000000000000000000, -1.734723475976806848E-16, 0.000000000000000000 ) ) ;
#3281=DIRECTION ( 'NONE',  ( -0.000000000000000000, -0.000000000000000000, 1.000000000000000000 ) ) ;
#3283=PLANE ( 'NONE',  #1674 ) ;
#3306=PLANE ( 'NONE',  #3128 ) ;
#3325=( LENGTH_UNIT ( ) NAMED_UNIT ( * ) SI_UNIT ( .MILLI., .METRE. ) );
#3336=LINE ( 'NONE', #3822, #7226 ) ;
#3356=LINE ( 'NONE', #8546, #4619 ) ;
#3369=DIRECTION ( 'NONE',  ( -1.734723475976806848E-16, -1.000000000000000000, 0.000000000000000000 ) ) ;
#3380=VECTOR ( 'NONE', #5251, 1000.000000000000000 ) ;
#3385=ORIENTED_EDGE ( 'NONE', *, *, #6459, .F. ) ;
#3413=PLANE ( 'NONE',  #1664 ) ;
#3418=ORIENTED_EDGE ( 'NONE', *, *, #6474, .T. ) ;
#3419=DIRECTION ( 'NONE',  ( 0.000000000000000000, 0.000000000000000000, -1.000000000000000000 ) ) ;
#3453=EDGE_CURVE ( 'NONE', #3816, #7049, #4303, .T. ) ;
#3454=EDGE_CURVE ( 'NONE', #5343, #6638, #3474, .T. ) ;
#3457=DIRECTION ( 'NONE',  ( 0.000000000000000000, 0.000000000000000000, 1.000000000000000000 ) ) ;
#3458=FACE_OUTER_BOUND ( 'NONE', #4986, .T. ) ;
#3463=ORIENTED_EDGE ( 'NONE', *, *, #704, .T. ) ;
#3474=CIRCLE ( 'NONE', #1948, 10.00000000000000000 ) ;
#3493=FACE_OUTER_BOUND ( 'NONE', #2183, .T. ) ;
#3498=DIRECTION ( 'NONE',  ( 1.000000000000000000, 0.000000000000000000, 0.000000000000000000 ) ) ;
#3512=FACE_OUTER_BOUND ( 'NONE', #4512, .T. ) ;
#3515=PRODUCT_DEFINITION ( 'UNKNOWN', '', #440, #4548 ) ;
#3516=ORIENTED_EDGE ( 'NONE', *, *, #4245, .F. ) ;
#3519=DIRECTION ( 'NONE',  ( 0.000000000000000000, 0.000000000000000000, -1.000000000000000000 ) ) ;
#3533=DIRECTION ( 'NONE',  ( 0.000000000000000000, 0.000000000000000000, 1.000000000000000000 ) ) ;
#3538=EDGE_CURVE ( 'NONE', #1033, #1781, #1893, .T. ) ;
#3576=VECTOR ( 'NONE', #2479, 1000.000000000000000 ) ;
#3598=CARTESIAN_POINT ( 'NONE',  ( -5.000000000000001776, 5.000000000000001776, 148.0000000000000284 ) ) ;
#3638=DIRECTION ( 'NONE',  ( 0.000000000000000000, 0.000000000000000000, -1.000000000000000000 ) ) ;
#3639=EDGE_CURVE ( 'NONE', #5674, #1367, #5266, .T. ) ;
#3641=EDGE_LOOP ( 'NONE', ( #5824, #5975, #1131, #7539 ) ) ;
#3701=VECTOR ( 'NONE', #6398, 1000.000000000000000 ) ;
#3733=DIRECTION ( 'NONE',  ( 1.000000000000000000, 0.000000000000000000, 0.000000000000000000 ) ) ;
#3753=ADVANCED_FACE ( 'NONE', ( #261 ), #348, .F. ) ;
#3779=CARTESIAN_POINT ( 'NONE',  ( 5.000000000000000000, -5.000000000000000000, -135.0000000000000000 ) ) ;
#3782=ADVANCED_FACE ( 'NONE', ( #3512 ), #1552, .T. ) ;
#3787=ORIENTED_EDGE ( 'NONE', *, *, #5195, .F. ) ;
#3807=VERTEX_POINT ( 'NONE', #8244 ) ;
#3816=VERTEX_POINT ( 'NONE', #7677 ) ;
#3817=SURFACE_SIDE_STYLE ('',( #5117 ) ) ;
#3820=ORIENTED_EDGE ( 'NONE', *, *, #450, .F. ) ;
#3822=CARTESIAN_POINT ( 'NONE',  ( 5.000000000000000000, -5.000000000000000000, 148.0000000000000284 ) ) ;
#3845=AXIS2_PLACEMENT_3D ( 'NONE', #7206, #4637, #3212 ) ;
#3854=DIRECTION ( 'NONE',  ( 1.000000000000000000, -1.734723475976806848E-16, 0.000000000000000000 ) ) ;
#3860=SHAPE_REPRESENTATION_RELATIONSHIP ( 'NONE' , 'NONE' ,  #1533, #7622 ) ;
#3863=EDGE_LOOP ( 'NONE', ( #1393, #2329, #3463, #909 ) ) ;
#3879=ADVANCED_FACE ( 'NONE', ( #4107 ), #3283, .F. ) ;
#3882=VERTEX_POINT ( 'NONE', #762 ) ;
#3893=LINE ( 'NONE', #1196, #6021 ) ;
#3924=LINE ( 'NONE', #1225, #1151 ) ;
#3930=CARTESIAN_POINT ( 'NONE',  ( 5.000000000000000000, -5.000000000000000000, -143.0000000000000284 ) ) ;
#3935=CARTESIAN_POINT ( 'NONE',  ( -5.000000000000001776, 5.000000000000001776, 148.0000000000000284 ) ) ;
#3940=CARTESIAN_POINT ( 'NONE',  ( -5.000000000000001776, 5.000000000000001776, -143.0000000000000284 ) ) ;
#3943=DIRECTION ( 'NONE',  ( -1.000000000000000000, 0.000000000000000000, 0.000000000000000000 ) ) ;
#3944=VECTOR ( 'NONE', #2908, 1000.000000000000000 ) ;
#3971=ORIENTED_EDGE ( 'NONE', *, *, #5195, .T. ) ;
#4010=VERTEX_POINT ( 'NONE', #4322 ) ;
#4016=ORIENTED_EDGE ( 'NONE', *, *, #5750, .F. ) ;
#4021=CARTESIAN_POINT ( 'NONE',  ( -10.00000000000000000, 1.224646799147353256E-15, 140.0000000000000000 ) ) ;
#4029=ORIENTED_EDGE ( 'NONE', *, *, #7307, .T. ) ;
#4033=EDGE_CURVE ( 'NONE', #3807, #7646, #6142, .T. ) ;
#4089=VECTOR ( 'NONE', #8260, 1000.000000000000000 ) ;
#4090=LINE ( 'NONE', #8229, #6703 ) ;
#4107=FACE_OUTER_BOUND ( 'NONE', #2596, .T. ) ;
#4144=DIRECTION ( 'NONE',  ( 0.000000000000000000, 0.000000000000000000, 1.000000000000000000 ) ) ;
#4157=ORIENTED_EDGE ( 'NONE', *, *, #6430, .F. ) ;
#4168=EDGE_CURVE ( 'NONE', #8492, #1599, #4279, .T. ) ;
#4182=ORIENTED_EDGE ( 'NONE', *, *, #1919, .F. ) ;
#4204=DIRECTION ( 'NONE',  ( 1.000000000000000000, 0.000000000000000000, 0.000000000000000000 ) ) ;
#4245=EDGE_CURVE ( 'NONE', #8587, #8492, #7728, .T. ) ;
#4266=ORIENTED_EDGE ( 'NONE', *, *, #7307, .F. ) ;
#4272=DIRECTION ( 'NONE',  ( 0.000000000000000000, 0.000000000000000000, 1.000000000000000000 ) ) ;
#4276=DIRECTION ( 'NONE',  ( 1.000000000000000000, 0.000000000000000000, 0.000000000000000000 ) ) ;
#4279=LINE ( 'NONE', #1585, #840 ) ;
#4292=EDGE_LOOP ( 'NONE', ( #4157, #4893, #7142, #3385 ) ) ;
#4303=CIRCLE ( 'NONE', #971, 20.00000000000000000 ) ;
#4321=DIRECTION ( 'NONE',  ( -1.734723475976806848E-16, 1.000000000000000000, 0.000000000000000000 ) ) ;
#4322=CARTESIAN_POINT ( 'NONE',  ( -10.00000000000000000, 1.224646799147353256E-15, -135.0000000000000000 ) ) ;
#4351=AXIS2_PLACEMENT_3D ( 'NONE', #1510, #5380, #4204 ) ;
#4384=EDGE_LOOP ( 'NONE', ( #395, #6384 ) ) ;
#4394=FACE_BOUND ( 'NONE', #2147, .T. ) ;
#4401=CARTESIAN_POINT ( 'NONE',  ( 10.00000000000000000, 0.000000000000000000, -135.0000000000000000 ) ) ;
#4427=DIRECTION ( 'NONE',  ( 1.734723475976806848E-16, -1.000000000000000000, -0.000000000000000000 ) ) ;
#4436=ORIENTED_EDGE ( 'NONE', *, *, #8204, .F. ) ;
#4442=ADVANCED_FACE ( 'NONE', ( #6914, #4394 ), #340, .F. ) ;
#4468=CARTESIAN_POINT ( 'NONE',  ( -5.000000000000000000, -5.000000000000000000, 148.0000000000000284 ) ) ;
#4473=EDGE_CURVE ( 'NONE', #3882, #5424, #21, .T. ) ;
#4480=VECTOR ( 'NONE', #3498, 1000.000000000000000 ) ;
#4500=DIRECTION ( 'NONE',  ( -0.000000000000000000, -0.000000000000000000, 1.000000000000000000 ) ) ;
#4512=EDGE_LOOP ( 'NONE', ( #1163, #7397, #84, #3820 ) ) ;
#4548=PRODUCT_DEFINITION_CONTEXT ( 'detailed design', #2860, 'design' ) ;
#4550=ORIENTED_EDGE ( 'NONE', *, *, #5176, .T. ) ;
#4576=CARTESIAN_POINT ( 'NONE',  ( 0.000000000000000000, 0.000000000000000000, -115.0000000000000000 ) ) ;
#4584=ORIENTED_EDGE ( 'NONE', *, *, #3194, .T. ) ;
#4613=AXIS2_PLACEMENT_3D ( 'NONE', #5013, #1673, #4321 ) ;
#4619=VECTOR ( 'NONE', #747, 1000.000000000000000 ) ;
#4636=CIRCLE ( 'NONE', #1302, 20.00000000000000000 ) ;
#4637=DIRECTION ( 'NONE',  ( 1.000000000000000000, 1.734723475976806848E-16, -0.000000000000000000 ) ) ;
#4639=CARTESIAN_POINT ( 'NONE',  ( 5.000000000000000000, 5.000000000000000000, 148.0000000000000284 ) ) ;
#4668=DIRECTION ( 'NONE',  ( 1.000000000000000000, 0.000000000000000000, 0.000000000000000000 ) ) ;
#4680=AXIS2_PLACEMENT_3D ( 'NONE', #8439, #2517, #2562 ) ;
#4711=AXIS2_PLACEMENT_3D ( 'NONE', #5970, #8038, #4668 ) ;
#4712=( NAMED_UNIT ( * ) SI_UNIT ( $, .STERADIAN. ) SOLID_ANGLE_UNIT ( ) );
#4757=MANIFOLD_SOLID_BREP ( 'Boss-Extrude4', #7600 ) ;
#4763=ADVANCED_FACE ( 'NONE', ( #7066 ), #6751, .F. ) ;
#4765=VERTEX_POINT ( 'NONE', #5403 ) ;
#4794=DIRECTION ( 'NONE',  ( -1.000000000000000000, 0.000000000000000000, -0.000000000000000000 ) ) ;
#4820=ORIENTED_EDGE ( 'NONE', *, *, #7346, .F. ) ;
#4826=EDGE_CURVE ( 'NONE', #5500, #1781, #3096, .T. ) ;
#4843=DIRECTION ( 'NONE',  ( 0.000000000000000000, -0.000000000000000000, 1.000000000000000000 ) ) ;
#4893=ORIENTED_EDGE ( 'NONE', *, *, #491, .F. ) ;
#4898=EDGE_LOOP ( 'NONE', ( #773, #2579, #4029, #2391 ) ) ;
#4907=EDGE_LOOP ( 'NONE', ( #3418, #4016, #4266, #3971 ) ) ;
#4924=VECTOR ( 'NONE', #3854, 1000.000000000000000 ) ;
#4930=CIRCLE ( 'NONE', #6026, 10.00000000000000000 ) ;
#4941=DIRECTION ( 'NONE',  ( -0.000000000000000000, 0.000000000000000000, 1.000000000000000000 ) ) ;
#4958=ORIENTED_EDGE ( 'NONE', *, *, #279, .F. ) ;
#4970=EDGE_CURVE ( 'NONE', #2803, #242, #8115, .T. ) ;
#4986=EDGE_LOOP ( 'NONE', ( #2856, #2395, #847, #1687 ) ) ;
#5012=PLANE ( 'NONE',  #2820 ) ;
#5013=CARTESIAN_POINT ( 'NONE',  ( -5.000000000000000000, -5.000000000000000000, -143.0000000000000284 ) ) ;
#5020=CARTESIAN_POINT ( 'NONE',  ( 5.000000000000000000, 5.000000000000000000, -143.0000000000000284 ) ) ;
#5036=CIRCLE ( 'NONE', #308, 20.00000000000000000 ) ;
#5039=ORIENTED_EDGE ( 'NONE', *, *, #7605, .T. ) ;
#5040=VECTOR ( 'NONE', #8422, 1000.000000000000000 ) ;
#5053=VERTEX_POINT ( 'NONE', #5621 ) ;
#5055=DIRECTION ( 'NONE',  ( 0.000000000000000000, 0.000000000000000000, -1.000000000000000000 ) ) ;
#5070=VERTEX_POINT ( 'NONE', #352 ) ;
#5099=ADVANCED_FACE ( 'NONE', ( #3018 ), #5012, .T. ) ;
#5108=CARTESIAN_POINT ( 'NONE',  ( 0.000000000000000000, 0.000000000000000000, -135.0000000000000000 ) ) ;
#5117=SURFACE_STYLE_FILL_AREA ( #7160 ) ;
#5126=EDGE_CURVE ( 'NONE', #4010, #5500, #8334, .T. ) ;
#5145=AXIS2_PLACEMENT_3D ( 'NONE', #3002, #7620, #5609 ) ;
#5155=( NAMED_UNIT ( * ) PLANE_ANGLE_UNIT ( ) SI_UNIT ( $, .RADIAN. ) );
#5156=CARTESIAN_POINT ( 'NONE',  ( 10.00000000000000000, 0.000000000000000000, -135.0000000000000000 ) ) ;
#5164=CYLINDRICAL_SURFACE ( 'NONE', #6147, 20.00000000000000000 ) ;
#5167=DIRECTION ( 'NONE',  ( -0.000000000000000000, -0.000000000000000000, 1.000000000000000000 ) ) ;
#5175=ORIENTED_EDGE ( 'NONE', *, *, #3538, .F. ) ;
#5176=EDGE_CURVE ( 'NONE', #5424, #1367, #3924, .T. ) ;
#5195=EDGE_CURVE ( 'NONE', #1599, #4765, #3356, .T. ) ;
#5199=( LENGTH_UNIT ( ) NAMED_UNIT ( * ) SI_UNIT ( .MILLI., .METRE. ) );
#5230=AXIS2_PLACEMENT_3D ( 'NONE', #8288, #3533, #1666 ) ;
#5248=EDGE_LOOP ( 'NONE', ( #2915, #8010, #1715, #5175 ) ) ;
#5251=DIRECTION ( 'NONE',  ( -1.000000000000000000, 1.734723475976806848E-16, -0.000000000000000000 ) ) ;
#5254=DIRECTION ( 'NONE',  ( 0.000000000000000000, 0.000000000000000000, -1.000000000000000000 ) ) ;
#5266=LINE ( 'NONE', #3930, #7216 ) ;
#5272=VECTOR ( 'NONE', #7768, 1000.000000000000000 ) ;
#5277=PRESENTATION_STYLE_ASSIGNMENT (( #1238 ) ) ;
#5301=ORIENTED_EDGE ( 'NONE', *, *, #6187, .F. ) ;
#5302=STYLED_ITEM('',(#8678),#4757);
#5307=DIRECTION ( 'NONE',  ( 0.000000000000000000, 0.000000000000000000, -1.000000000000000000 ) ) ;
#5343=VERTEX_POINT ( 'NONE', #6743 ) ;
#5377=ORIENTED_EDGE ( 'NONE', *, *, #5677, .T. ) ;
#5379=ORIENTED_EDGE ( 'NONE', *, *, #5750, .T. ) ;
#5380=DIRECTION ( 'NONE',  ( -0.000000000000000000, -0.000000000000000000, 1.000000000000000000 ) ) ;
#5403=CARTESIAN_POINT ( 'NONE',  ( -5.000000000000001776, 5.000000000000001776, 140.0000000000000000 ) ) ;
#5424=VERTEX_POINT ( 'NONE', #1133 ) ;
#5440=CARTESIAN_POINT ( 'NONE',  ( 0.000000000000000000, 0.000000000000000000, 120.0000000000000142 ) ) ;
#5456=DIRECTION ( 'NONE',  ( 0.000000000000000000, 0.000000000000000000, 1.000000000000000000 ) ) ;
#5500=VERTEX_POINT ( 'NONE', #481 ) ;
#5543=CARTESIAN_POINT ( 'NONE',  ( 0.000000000000000000, 0.000000000000000000, 120.0000000000000142 ) ) ;
#5550=LINE ( 'NONE', #326, #5644 ) ;
#5584=CARTESIAN_POINT ( 'NONE',  ( -5.000000000000000000, -5.000000000000000000, -135.0000000000000000 ) ) ;
#5592=CARTESIAN_POINT ( 'NONE',  ( 0.000000000000000000, 0.000000000000000000, -191.5685424949238325 ) ) ;
#5604=CARTESIAN_POINT ( 'NONE',  ( -20.00000000000000000, 2.449293598294706513E-15, 120.0000000000000142 ) ) ;
#5608=AXIS2_PLACEMENT_3D ( 'NONE', #5020, #1111, #4941 ) ;
#5609=DIRECTION ( 'NONE',  ( -1.000000000000000000, 0.000000000000000000, -0.000000000000000000 ) ) ;
#5621=CARTESIAN_POINT ( 'NONE',  ( -5.000000000000000000, -5.000000000000000000, 140.0000000000000000 ) ) ;
#5622=FACE_OUTER_BOUND ( 'NONE', #7487, .T. ) ;
#5644=VECTOR ( 'NONE', #1734, 1000.000000000000000 ) ;
#5673=EDGE_LOOP ( 'NONE', ( #2821, #1661, #4958, #663 ) ) ;
#5674=VERTEX_POINT ( 'NONE', #605 ) ;
#5677=EDGE_CURVE ( 'NONE', #2732, #4765, #6520, .T. ) ;
#5691=ORIENTED_EDGE ( 'NONE', *, *, #3454, .F. ) ;
#5728=CARTESIAN_POINT ( 'NONE',  ( -5.000000000000000000, -5.000000000000000000, -135.0000000000000000 ) ) ;
#5740=VECTOR ( 'NONE', #5167, 1000.000000000000000 ) ;
#5741=EDGE_CURVE ( 'NONE', #6638, #5343, #2008, .T. ) ;
#5748=CARTESIAN_POINT ( 'NONE',  ( -10.00000000000000000, 1.224646799147353256E-15, -135.0000000000000000 ) ) ;
#5750=EDGE_CURVE ( 'NONE', #2805, #5053, #4090, .T. ) ;
#5764=DIRECTION ( 'NONE',  ( 1.000000000000000000, 0.000000000000000000, 0.000000000000000000 ) ) ;
#5765=FACE_OUTER_BOUND ( 'NONE', #5673, .T. ) ;
#5770=DIRECTION ( 'NONE',  ( 0.000000000000000000, 1.000000000000000000, 0.000000000000000000 ) ) ;
#5824=ORIENTED_EDGE ( 'NONE', *, *, #6459, .T. ) ;
#5842=LINE ( 'NONE', #7822, #3576 ) ;
#5860=CARTESIAN_POINT ( 'NONE',  ( -20.00000000000000000, 2.449293598294706513E-15, -115.0000000000000000 ) ) ;
#5917=ADVANCED_FACE ( 'NONE', ( #7122 ), #6297, .T. ) ;
#5970=CARTESIAN_POINT ( 'NONE',  ( 0.000000000000000000, 0.000000000000000000, -135.0000000000000000 ) ) ;
#5975=ORIENTED_EDGE ( 'NONE', *, *, #4473, .F. ) ;
#5993=( GEOMETRIC_REPRESENTATION_CONTEXT ( 3 ) GLOBAL_UNCERTAINTY_ASSIGNED_CONTEXT ( ( #767 ) ) GLOBAL_UNIT_ASSIGNED_CONTEXT ( ( #3325, #2586, #4712 ) ) REPRESENTATION_CONTEXT ( 'NONE', 'WORKASPACE' ) );
#6000=VECTOR ( 'NONE', #3281, 1000.000000000000000 ) ;
#6013=CARTESIAN_POINT ( 'NONE',  ( 0.000000000000000000, 0.000000000000000000, -135.0000000000000000 ) ) ;
#6021=VECTOR ( 'NONE', #3200, 1000.000000000000000 ) ;
#6022=ORIENTED_EDGE ( 'NONE', *, *, #5677, .F. ) ;
#6026=AXIS2_PLACEMENT_3D ( 'NONE', #1606, #6115, #6819 ) ;
#6040=DIRECTION ( 'NONE',  ( -1.000000000000000000, 0.000000000000000000, 0.000000000000000000 ) ) ;
#6103=EDGE_CURVE ( 'NONE', #8587, #7465, #3336, .T. ) ;
#6114=DIRECTION ( 'NONE',  ( -1.000000000000000000, 0.000000000000000000, 0.000000000000000000 ) ) ;
#6115=DIRECTION ( 'NONE',  ( 0.000000000000000000, 0.000000000000000000, -1.000000000000000000 ) ) ;
#6123=EDGE_LOOP ( 'NONE', ( #4182, #2994, #5039, #8091 ) ) ;
#6142=LINE ( 'NONE', #7545, #6945 ) ;
#6147=AXIS2_PLACEMENT_3D ( 'NONE', #515, #3174, #6514 ) ;
#6154=MECHANICAL_DESIGN_GEOMETRIC_PRESENTATION_REPRESENTATION('',(#7139),#177);
#6165=CIRCLE ( 'NONE', #2144, 10.00000000000000000 ) ;
#6187=EDGE_CURVE ( 'NONE', #1781, #5500, #6165, .T. ) ;
#6191=ORIENTED_EDGE ( 'NONE', *, *, #6430, .T. ) ;
#6212=AXIS2_PLACEMENT_3D ( 'NONE', #2753, #6699, #660 ) ;
#6241=PLANE ( 'NONE',  #5608 ) ;
#6242=EDGE_CURVE ( 'NONE', #2989, #3079, #4636, .T. ) ;
#6297=CYLINDRICAL_SURFACE ( 'NONE', #211, 10.00000000000000000 ) ;
#6307=ADVANCED_FACE ( 'NONE', ( #320 ), #6241, .F. ) ;
#6315=CARTESIAN_POINT ( 'NONE',  ( -5.000000000000000000, -5.000000000000000000, 148.0000000000000284 ) ) ;
#6328=CARTESIAN_POINT ( 'NONE',  ( 20.00000000000000000, 0.000000000000000000, -191.5685424949238325 ) ) ;
#6329=EDGE_LOOP ( 'NONE', ( #5301, #2461 ) ) ;
#6384=ORIENTED_EDGE ( 'NONE', *, *, #666, .F. ) ;
#6398=DIRECTION ( 'NONE',  ( -0.000000000000000000, -0.000000000000000000, 1.000000000000000000 ) ) ;
#6417=MECHANICAL_DESIGN_GEOMETRIC_PRESENTATION_REPRESENTATION('',(#5302),#5993);
#6419=CARTESIAN_POINT ( 'NONE',  ( 10.00000000000000000, 0.000000000000000000, -115.0000000000000000 ) ) ;
#6430=EDGE_CURVE ( 'NONE', #1428, #5070, #7556, .T. ) ;
#6444=VECTOR ( 'NONE', #7108, 1000.000000000000000 ) ;
#6450=VECTOR ( 'NONE', #3280, 1000.000000000000000 ) ;
#6459=EDGE_CURVE ( 'NONE', #5070, #5424, #2473, .T. ) ;
#6461=ADVANCED_FACE ( 'NONE', ( #6623 ), #537, .T. ) ;
#6472=ORIENTED_EDGE ( 'NONE', *, *, #4473, .T. ) ;
#6474=EDGE_CURVE ( 'NONE', #4765, #5053, #7231, .T. ) ;
#6482=EDGE_CURVE ( 'NONE', #7646, #3882, #7894, .T. ) ;
#6514=DIRECTION ( 'NONE',  ( 1.000000000000000000, 0.000000000000000000, 0.000000000000000000 ) ) ;
#6519=ORIENTED_EDGE ( 'NONE', *, *, #1043, .T. ) ;
#6520=LINE ( 'NONE', #559, #3380 ) ;
#6529=EDGE_CURVE ( 'NONE', #242, #6638, #3893, .T. ) ;
#6535=CARTESIAN_POINT ( 'NONE',  ( -5.000000000000000000, -5.000000000000000000, 140.0000000000000000 ) ) ;
#6548=PLANE ( 'NONE',  #3845 ) ;
#6585=DIRECTION ( 'NONE',  ( 1.000000000000000000, -1.734723475976806848E-16, 0.000000000000000000 ) ) ;
#6614=PLANE ( 'NONE',  #2050 ) ;
#6623=FACE_OUTER_BOUND ( 'NONE', #1216, .T. ) ;
#6629=( LENGTH_UNIT ( ) NAMED_UNIT ( * ) SI_UNIT ( .MILLI., .METRE. ) );
#6638=VERTEX_POINT ( 'NONE', #4021 ) ;
#6665=CARTESIAN_POINT ( 'NONE',  ( -5.000000000000001776, 5.000000000000001776, -143.0000000000000284 ) ) ;
#6671=UNCERTAINTY_MEASURE_WITH_UNIT (LENGTH_MEASURE( 1.000000000000000082E-05 ), #6629, 'distance_accuracy_value', 'NONE');
#6677=ORIENTED_EDGE ( 'NONE', *, *, #7146, .T. ) ;
#6699=DIRECTION ( 'NONE',  ( 0.000000000000000000, 0.000000000000000000, 1.000000000000000000 ) ) ;
#6703=VECTOR ( 'NONE', #8056, 1000.000000000000000 ) ;
#6710=CYLINDRICAL_SURFACE ( 'NONE', #4711, 10.00000000000000000 ) ;
#6743=CARTESIAN_POINT ( 'NONE',  ( 10.00000000000000000, 0.000000000000000000, 140.0000000000000000 ) ) ;
#6748=ORIENTED_EDGE ( 'NONE', *, *, #4033, .F. ) ;
#6751=PLANE ( 'NONE',  #8247 ) ;
#6819=DIRECTION ( 'NONE',  ( -1.000000000000000000, 0.000000000000000000, 0.000000000000000000 ) ) ;
#6854=DIRECTION ( 'NONE',  ( -1.000000000000000000, 0.000000000000000000, 0.000000000000000000 ) ) ;
#6858=AXIS2_PLACEMENT_3D ( 'NONE', #2822, #3519, #6114 ) ;
#6862=DIRECTION ( 'NONE',  ( -1.000000000000000000, 0.000000000000000000, -0.000000000000000000 ) ) ;
#6873=CARTESIAN_POINT ( 'NONE',  ( 0.000000000000000000, 0.000000000000000000, -115.0000000000000000 ) ) ;
#6881=DIRECTION ( 'NONE',  ( 1.000000000000000000, 0.000000000000000000, 0.000000000000000000 ) ) ;
#6882=EDGE_LOOP ( 'NONE', ( #4550, #7418, #2766, #6472 ) ) ;
#6914=FACE_OUTER_BOUND ( 'NONE', #1290, .T. ) ;
#6915=ORIENTED_EDGE ( 'NONE', *, *, #3194, .F. ) ;
#6945=VECTOR ( 'NONE', #7454, 1000.000000000000000 ) ;
#6993=ADVANCED_FACE ( 'NONE', ( #8579, #7304 ), #3306, .T. ) ;
#7024=EDGE_LOOP ( 'NONE', ( #4584, #6677 ) ) ;
#7037=CARTESIAN_POINT ( 'NONE',  ( 0.000000000000000000, 0.000000000000000000, -135.0000000000000000 ) ) ;
#7049=VERTEX_POINT ( 'NONE', #5860 ) ;
#7052=LINE ( 'NONE', #1095, #3701 ) ;
#7065=AXIS2_PLACEMENT_3D ( 'NONE', #5440, #4272, #6881 ) ;
#7066=FACE_OUTER_BOUND ( 'NONE', #7159, .T. ) ;
#7075=DIRECTION ( 'NONE',  ( -0.000000000000000000, -0.000000000000000000, 1.000000000000000000 ) ) ;
#7080=VECTOR ( 'NONE', #2466, 1000.000000000000000 ) ;
#7103=CARTESIAN_POINT ( 'NONE',  ( 10.00000000000000000, 0.000000000000000000, -135.0000000000000000 ) ) ;
#7108=DIRECTION ( 'NONE',  ( 0.000000000000000000, 0.000000000000000000, 1.000000000000000000 ) ) ;
#7122=FACE_OUTER_BOUND ( 'NONE', #5248, .T. ) ;
#7139=STYLED_ITEM ( 'NONE', ( #5277 ), #7622 ) ;
#7142=ORIENTED_EDGE ( 'NONE', *, *, #5176, .F. ) ;
#7144=ORIENTED_EDGE ( 'NONE', *, *, #6103, .F. ) ;
#7146=EDGE_CURVE ( 'NONE', #4010, #1033, #4930, .T. ) ;
#7155=EDGE_CURVE ( 'NONE', #8492, #2732, #2823, .T. ) ;
#7159=EDGE_LOOP ( 'NONE', ( #5377, #3787, #7929, #2107 ) ) ;
#7160=FILL_AREA_STYLE ('',( #7199 ) ) ;
#7199=FILL_AREA_STYLE_COLOUR ( '', #2137 ) ;
#7206=CARTESIAN_POINT ( 'NONE',  ( -5.000000000000000000, -5.000000000000000000, 148.0000000000000284 ) ) ;
#7216=VECTOR ( 'NONE', #42, 1000.000000000000000 ) ;
#7226=VECTOR ( 'NONE', #3169, 1000.000000000000000 ) ;
#7231=LINE ( 'NONE', #6535, #8127 ) ;
#7273=FACE_OUTER_BOUND ( 'NONE', #4898, .T. ) ;
#7289=( NAMED_UNIT ( * ) PLANE_ANGLE_UNIT ( ) SI_UNIT ( $, .RADIAN. ) );
#7304=FACE_OUTER_BOUND ( 'NONE', #8148, .T. ) ;
#7307=EDGE_CURVE ( 'NONE', #1599, #2805, #470, .T. ) ;
#7324=VECTOR ( 'NONE', #617, 1000.000000000000000 ) ;
#7346=EDGE_CURVE ( 'NONE', #7465, #2732, #8406, .T. ) ;
#7357=DIRECTION ( 'NONE',  ( 0.000000000000000000, -1.000000000000000000, 0.000000000000000000 ) ) ;
#7367=EDGE_CURVE ( 'NONE', #2805, #8587, #1826, .T. ) ;
#7375=UNCERTAINTY_MEASURE_WITH_UNIT (LENGTH_MEASURE( 1.000000000000000082E-05 ), #5199, 'distance_accuracy_value', 'NONE');
#7397=ORIENTED_EDGE ( 'NONE', *, *, #6529, .T. ) ;
#7418=ORIENTED_EDGE ( 'NONE', *, *, #3639, .F. ) ;
#7454=DIRECTION ( 'NONE',  ( -1.734723475976806848E-16, 1.000000000000000000, 0.000000000000000000 ) ) ;
#7465=VERTEX_POINT ( 'NONE', #1327 ) ;
#7487=EDGE_LOOP ( 'NONE', ( #6191, #2123, #6748, #6519 ) ) ;
#7539=ORIENTED_EDGE ( 'NONE', *, *, #7795, .T. ) ;
#7545=CARTESIAN_POINT ( 'NONE',  ( -5.000000000000000000, -5.000000000000000000, -143.0000000000000284 ) ) ;
#7556=LINE ( 'NONE', #5584, #4089 ) ;
#7600=CLOSED_SHELL ( 'NONE', ( #3782, #8440, #5917, #6461, #223, #8124, #3273, #6307, #484, #5099, #6993, #824, #329, #708, #4763, #1473, #3753, #3879, #4442, #3191 ) ) ;
#7605=EDGE_CURVE ( 'NONE', #3816, #2989, #321, .T. ) ;
#7620=DIRECTION ( 'NONE',  ( 0.000000000000000000, 0.000000000000000000, -1.000000000000000000 ) ) ;
#7622=ADVANCED_BREP_SHAPE_REPRESENTATION ( '', ( #4757, #594 ), #1167 ) ;
#7627=PLANE ( 'NONE',  #5230 ) ;
#7646=VERTEX_POINT ( 'NONE', #8431 ) ;
#7677=CARTESIAN_POINT ( 'NONE',  ( 20.00000000000000000, 0.000000000000000000, -115.0000000000000000 ) ) ;
#7711=AXIS2_PLACEMENT_3D ( 'NONE', #5108, #4500, #2552 ) ;
#7728=LINE ( 'NONE', #2465, #5272 ) ;
#7745=DIRECTION ( 'NONE',  ( -0.000000000000000000, -0.000000000000000000, 1.000000000000000000 ) ) ;
#7746=CARTESIAN_POINT ( 'NONE',  ( -5.000000000000000000, -5.000000000000000000, 148.0000000000000284 ) ) ;
#7768=DIRECTION ( 'NONE',  ( 0.000000000000000000, 1.000000000000000000, 0.000000000000000000 ) ) ;
#7795=EDGE_CURVE ( 'NONE', #7646, #5070, #7941, .T. ) ;
#7822=CARTESIAN_POINT ( 'NONE',  ( 5.000000000000000000, -5.000000000000000000, -135.0000000000000000 ) ) ;
#7853=VECTOR ( 'NONE', #4427, 1000.000000000000000 ) ;
#7892=DIRECTION ( 'NONE',  ( 1.000000000000000000, -1.734723475976806848E-16, 0.000000000000000000 ) ) ;
#7894=LINE ( 'NONE', #1898, #4924 ) ;
#7929=ORIENTED_EDGE ( 'NONE', *, *, #4168, .F. ) ;
#7941=LINE ( 'NONE', #3940, #6000 ) ;
#7953=PRODUCT ( 'roller axis assy_r1', 'roller axis assy_r1', '', ( #1425 ) ) ;
#7959=CARTESIAN_POINT ( 'NONE',  ( -20.00000000000000000, 2.449293598294706513E-15, -191.5685424949238325 ) ) ;
#8010=ORIENTED_EDGE ( 'NONE', *, *, #5126, .T. ) ;
#8020=EDGE_CURVE ( 'NONE', #5053, #7465, #1403, .T. ) ;
#8038=DIRECTION ( 'NONE',  ( -0.000000000000000000, -0.000000000000000000, 1.000000000000000000 ) ) ;
#8056=DIRECTION ( 'NONE',  ( -0.000000000000000000, -0.000000000000000000, -1.000000000000000000 ) ) ;
#8062=CARTESIAN_POINT ( 'NONE',  ( 20.00000000000000000, 0.000000000000000000, 120.0000000000000142 ) ) ;
#8079=CARTESIAN_POINT ( 'NONE',  ( -5.000000000000000000, -5.000000000000000000, 140.0000000000000000 ) ) ;
#8086=DIRECTION ( 'NONE',  ( 1.000000000000000000, 0.000000000000000000, 0.000000000000000000 ) ) ;
#8091=ORIENTED_EDGE ( 'NONE', *, *, #2603, .F. ) ;
#8094=CARTESIAN_POINT ( 'NONE',  ( 5.000000000000000000, -5.000000000000000000, 148.0000000000000284 ) ) ;
#8115=CIRCLE ( 'NONE', #1566, 10.00000000000000000 ) ;
#8124=ADVANCED_FACE ( 'NONE', ( #5622 ), #8337, .F. ) ;
#8127=VECTOR ( 'NONE', #669, 1000.000000000000000 ) ;
#8148=EDGE_LOOP ( 'NONE', ( #1777, #4436 ) ) ;
#8175=PRODUCT_DEFINITION_SHAPE ( 'NONE', 'NONE',  #3515 ) ;
#8204=EDGE_CURVE ( 'NONE', #7049, #3816, #5036, .T. ) ;
#8229=CARTESIAN_POINT ( 'NONE',  ( -5.000000000000000000, -5.000000000000000000, 148.0000000000000284 ) ) ;
#8230=CARTESIAN_POINT ( 'NONE',  ( 5.000000000000000000, 5.000000000000000000, 148.0000000000000284 ) ) ;
#8243=EDGE_LOOP ( 'NONE', ( #1817, #1056, #1668, #3206 ) ) ;
#8244=CARTESIAN_POINT ( 'NONE',  ( -5.000000000000000000, -5.000000000000000000, -143.0000000000000284 ) ) ;
#8247=AXIS2_PLACEMENT_3D ( 'NONE', #3935, #3278, #7892 ) ;
#8256=VECTOR ( 'NONE', #5770, 1000.000000000000000 ) ;
#8260=DIRECTION ( 'NONE',  ( -1.734723475976806848E-16, 1.000000000000000000, 0.000000000000000000 ) ) ;
#8288=CARTESIAN_POINT ( 'NONE',  ( 0.000000000000000000, 0.000000000000000000, 120.0000000000000142 ) ) ;
#8303=AXIS2_PLACEMENT_3D ( 'NONE', #3040, #3638, #6862 ) ;
#8334=LINE ( 'NONE', #5748, #5040 ) ;
#8337=PLANE ( 'NONE',  #4613 ) ;
#8406=LINE ( 'NONE', #1080, #8256 ) ;
#8422=DIRECTION ( 'NONE',  ( -0.000000000000000000, -0.000000000000000000, 1.000000000000000000 ) ) ;
#8426=DIRECTION ( 'NONE',  ( 0.000000000000000000, 0.000000000000000000, -1.000000000000000000 ) ) ;
#8431=CARTESIAN_POINT ( 'NONE',  ( -5.000000000000001776, 5.000000000000001776, -143.0000000000000284 ) ) ;
#8439=CARTESIAN_POINT ( 'NONE',  ( 5.000000000000000000, -5.000000000000000000, -143.0000000000000284 ) ) ;
#8440=ADVANCED_FACE ( 'NONE', ( #8528 ), #5164, .T. ) ;
#8492=VERTEX_POINT ( 'NONE', #4639 ) ;
#8515=( NAMED_UNIT ( * ) SI_UNIT ( $, .STERADIAN. ) SOLID_ANGLE_UNIT ( ) );
#8528=FACE_OUTER_BOUND ( 'NONE', #8243, .T. ) ;
#8546=CARTESIAN_POINT ( 'NONE',  ( -5.000000000000001776, 5.000000000000001776, 148.0000000000000284 ) ) ;
#8551=DIRECTION ( 'NONE',  ( -1.000000000000000000, 0.000000000000000000, 0.000000000000000000 ) ) ;
#8579=FACE_BOUND ( 'NONE', #6329, .T. ) ;
#8587=VERTEX_POINT ( 'NONE', #8094 ) ;
#8672=COLOUR_RGB('Off White',0.89,0.88,0.83);
#8673=FILL_AREA_STYLE_COLOUR('',#8672);
#8674=FILL_AREA_STYLE('',(#8673));
#8675=SURFACE_STYLE_FILL_AREA(#8674);
#8676=SURFACE_SIDE_STYLE('',(#8675));
#8677=SURFACE_STYLE_USAGE(.BOTH.,#8676);
#8678=PRESENTATION_STYLE_ASSIGNMENT((#8677));
ENDSEC;
END-ISO-10303-21;
